ISO-10303-21;
HEADER;
/* Generated by software containing ST-Developer
 * from STEP Tools, Inc. (www.steptools.com) 
 */

FILE_DESCRIPTION(
/* description */ ('Compact intermittent indexer'),
/* implementation_level */ '2;1');

FILE_NAME(
/* name */ 'Lower bearing sleeve (1).step',
/* time_stamp */ '2026-10-29T16:32:17-07:00',
/* author */ (''),
/* organization */ (''),
/* preprocessor_version */ 'ST-DEVELOPER v20.2',
/* originating_system */ 'Autodesk Translation Framework v15.17.0.0',
/* authorisation */ '');

FILE_SCHEMA (('AUTOMOTIVE_DESIGN { 1 0 10303 214 3 1 1 }'));
ENDSEC;

DATA;
#10=MECHANICAL_DESIGN_GEOMETRIC_PRESENTATION_REPRESENTATION('',(#286),#10837);
#230=SHAPE_REPRESENTATION_RELATIONSHIP('SRR','None',#10967,#254);
#254=ADVANCED_BREP_SHAPE_REPRESENTATION('',(#316),#10834);
#286=STYLED_ITEM('',(#11166),#316);
#316=MANIFOLD_SOLID_BREP('Body1',#5660);
#464=FACE_BOUND('',#1403,.T.);
#465=FACE_BOUND('',#1405,.T.);
#635=PLANE('',#6612);
#636=PLANE('',#6613);
#961=FACE_OUTER_BOUND('',#1400,.T.);
#962=FACE_OUTER_BOUND('',#1401,.T.);
#963=FACE_OUTER_BOUND('',#1402,.T.);
#964=FACE_OUTER_BOUND('',#1404,.T.);
#1400=EDGE_LOOP('',(#5056,#5057,#5058,#5059));
#1401=EDGE_LOOP('',(#5060,#5061,#5062,#5063));
#1402=EDGE_LOOP('',(#5064));
#1403=EDGE_LOOP('',(#5065));
#1404=EDGE_LOOP('',(#5066));
#1405=EDGE_LOOP('',(#5067));
#1758=LINE('',#10520,#2116);
#1759=LINE('',#10526,#2117);
#2116=VECTOR('',#8352,0.505);
#2117=VECTOR('',#8359,0.7);
#2466=CIRCLE('',#6607,0.505);
#2467=CIRCLE('',#6608,0.505);
#2468=CIRCLE('',#6610,0.7);
#2469=CIRCLE('',#6611,0.7);
#2938=VERTEX_POINT('',#10517);
#2939=VERTEX_POINT('',#10519);
#2940=VERTEX_POINT('',#10523);
#2941=VERTEX_POINT('',#10525);
#3650=EDGE_CURVE('',#2938,#2938,#2466,.T.);
#3651=EDGE_CURVE('',#2938,#2939,#1758,.T.);
#3652=EDGE_CURVE('',#2939,#2939,#2467,.T.);
#3653=EDGE_CURVE('',#2940,#2940,#2468,.T.);
#3654=EDGE_CURVE('',#2940,#2941,#1759,.T.);
#3655=EDGE_CURVE('',#2941,#2941,#2469,.T.);
#5056=ORIENTED_EDGE('',*,*,#3650,.F.);
#5057=ORIENTED_EDGE('',*,*,#3651,.T.);
#5058=ORIENTED_EDGE('',*,*,#3652,.T.);
#5059=ORIENTED_EDGE('',*,*,#3651,.F.);
#5060=ORIENTED_EDGE('',*,*,#3653,.F.);
#5061=ORIENTED_EDGE('',*,*,#3654,.T.);
#5062=ORIENTED_EDGE('',*,*,#3655,.T.);
#5063=ORIENTED_EDGE('',*,*,#3654,.F.);
#5064=ORIENTED_EDGE('',*,*,#3653,.T.);
#5065=ORIENTED_EDGE('',*,*,#3650,.T.);
#5066=ORIENTED_EDGE('',*,*,#3655,.F.);
#5067=ORIENTED_EDGE('',*,*,#3652,.F.);
#5288=CYLINDRICAL_SURFACE('',#6606,0.505);
#5289=CYLINDRICAL_SURFACE('',#6609,0.7);
#5604=ADVANCED_FACE('',(#961),#5288,.F.);
#5605=ADVANCED_FACE('',(#962),#5289,.T.);
#5606=ADVANCED_FACE('',(#963,#464),#635,.T.);
#5607=ADVANCED_FACE('',(#964,#465),#636,.F.);
#5660=CLOSED_SHELL('',(#5604,#5605,#5606,#5607));
#6605=AXIS2_PLACEMENT_3D('',#10515,#8346,#8347);
#6606=AXIS2_PLACEMENT_3D('',#10516,#8348,#8349);
#6607=AXIS2_PLACEMENT_3D('',#10518,#8350,#8351);
#6608=AXIS2_PLACEMENT_3D('',#10521,#8353,#8354);
#6609=AXIS2_PLACEMENT_3D('',#10522,#8355,#8356);
#6610=AXIS2_PLACEMENT_3D('',#10524,#8357,#8358);
#6611=AXIS2_PLACEMENT_3D('',#10527,#8360,#8361);
#6612=AXIS2_PLACEMENT_3D('',#10528,#8362,#8363);
#6613=AXIS2_PLACEMENT_3D('',#10529,#8364,#8365);
#8346=DIRECTION('axis',(0.,0.,1.));
#8347=DIRECTION('refdir',(1.,0.,0.));
#8348=DIRECTION('center_axis',(0.,0.,1.));
#8349=DIRECTION('ref_axis',(1.,0.,0.));
#8350=DIRECTION('center_axis',(0.,0.,-1.));
#8351=DIRECTION('ref_axis',(1.,0.,0.));
#8352=DIRECTION('',(0.,0.,-1.));
#8353=DIRECTION('center_axis',(0.,0.,-1.));
#8354=DIRECTION('ref_axis',(1.,0.,0.));
#8355=DIRECTION('center_axis',(0.,0.,1.));
#8356=DIRECTION('ref_axis',(1.,0.,0.));
#8357=DIRECTION('center_axis',(0.,0.,1.));
#8358=DIRECTION('ref_axis',(1.,0.,0.));
#8359=DIRECTION('',(0.,0.,-1.));
#8360=DIRECTION('center_axis',(0.,0.,1.));
#8361=DIRECTION('ref_axis',(1.,0.,0.));
#8362=DIRECTION('center_axis',(0.,0.,1.));
#8363=DIRECTION('ref_axis',(1.,0.,0.));
#8364=DIRECTION('center_axis',(0.,0.,1.));
#8365=DIRECTION('ref_axis',(1.,0.,0.));
#10515=CARTESIAN_POINT('',(0.,0.,0.));
#10516=CARTESIAN_POINT('Origin',(4.24264068711929,0.,1.8));
#10517=CARTESIAN_POINT('',(3.73764068711929,-6.18446633569413E-17,2.05));
#10518=CARTESIAN_POINT('Origin',(4.24264068711929,0.,2.05));
#10519=CARTESIAN_POINT('',(3.73764068711929,-6.18446633569413E-17,1.8));
#10520=CARTESIAN_POINT('',(3.73764068711929,-6.18446633569413E-17,1.8));
#10521=CARTESIAN_POINT('Origin',(4.24264068711929,0.,1.8));
#10522=CARTESIAN_POINT('Origin',(4.24264068711929,0.,1.8));
#10523=CARTESIAN_POINT('',(3.54264068711929,-8.57252759403147E-17,2.05));
#10524=CARTESIAN_POINT('Origin',(4.24264068711929,0.,2.05));
#10525=CARTESIAN_POINT('',(3.54264068711929,-8.57252759403147E-17,1.8));
#10526=CARTESIAN_POINT('',(3.54264068711929,-8.57252759403147E-17,1.8));
#10527=CARTESIAN_POINT('Origin',(4.24264068711929,0.,1.8));
#10528=CARTESIAN_POINT('Origin',(4.24264068711929,0.,2.05));
#10529=CARTESIAN_POINT('Origin',(4.24264068711929,0.,1.8));
#10804=UNCERTAINTY_MEASURE_WITH_UNIT(LENGTH_MEASURE(0.001),#10838,
'DISTANCE_ACCURACY_VALUE',
'Maximum model space distance between geometric entities at asserted c
onnectivities');
#10807=UNCERTAINTY_MEASURE_WITH_UNIT(LENGTH_MEASURE(0.001),#10838,
'DISTANCE_ACCURACY_VALUE',
'Maximum model space distance between geometric entities at asserted c
onnectivities');
#10834=(
GEOMETRIC_REPRESENTATION_CONTEXT(3)
GLOBAL_UNCERTAINTY_ASSIGNED_CONTEXT((#10804))
GLOBAL_UNIT_ASSIGNED_CONTEXT((#10838,#10840,#10841))
REPRESENTATION_CONTEXT('','3D')
);
#10837=(
GEOMETRIC_REPRESENTATION_CONTEXT(3)
GLOBAL_UNCERTAINTY_ASSIGNED_CONTEXT((#10807))
GLOBAL_UNIT_ASSIGNED_CONTEXT((#10838,#10840,#10841))
REPRESENTATION_CONTEXT('','3D')
);
#10838=(
LENGTH_UNIT()
NAMED_UNIT(*)
SI_UNIT(.CENTI.,.METRE.)
);
#10840=(
NAMED_UNIT(*)
PLANE_ANGLE_UNIT()
SI_UNIT($,.RADIAN.)
);
#10841=(
NAMED_UNIT(*)
SI_UNIT($,.STERADIAN.)
SOLID_ANGLE_UNIT()
);
#10868=SHAPE_DEFINITION_REPRESENTATION(#10921,#10967);
#10921=PRODUCT_DEFINITION_SHAPE('',$,#10997);
#10967=SHAPE_REPRESENTATION('',(#6605),#10834);
#10970=PRODUCT_DEFINITION_CONTEXT('part definition',#11059,'design');
#10997=PRODUCT_DEFINITION('Lower bearing sleeve (1)',
'Lower bearing sleeve (1)',#11026,#10970);
#11026=PRODUCT_DEFINITION_FORMATION('',$,#11087);
#11059=APPLICATION_CONTEXT(
'Core Data for Automotive Mechanical Design Process');
#11060=PRODUCT_CONTEXT('part definition',#11059,'mechanical');
#11087=PRODUCT('Lower bearing sleeve (1)','Lower bearing sleeve (1)',
'Lower bearing sleeve (1)',(#11060));
#11160=COLOUR_RGB('Grey',0.48,0.52,0.57);
#11161=FILL_AREA_STYLE_COLOUR('',#11160);
#11162=FILL_AREA_STYLE('',(#11161));
#11163=SURFACE_STYLE_FILL_AREA(#11162);
#11164=SURFACE_SIDE_STYLE('',(#11163));
#11165=SURFACE_STYLE_USAGE(.BOTH.,#11164);
#11166=PRESENTATION_STYLE_ASSIGNMENT((#11165));
ENDSEC;
END-ISO-10303-21;
